ISO-10303-21;
HEADER;
/* Generated by software containing ST-Developer
 * from STEP Tools, Inc. (www.steptools.com) 
 */

FILE_DESCRIPTION(
/* description */ ('Chain-less indexing wheel (Geneva) drive'),
/* implementation_level */ '2;1');

FILE_NAME(
/* name */ 'Retaining collar (1).step',
/* time_stamp */ '2026-10-28T03:25:22-07:00',
/* author */ (''),
/* organization */ (''),
/* preprocessor_version */ 'ST-DEVELOPER v20.2',
/* originating_system */ 'Autodesk Translation Framework v15.17.0.0',
/* authorisation */ '');

FILE_SCHEMA (('AUTOMOTIVE_DESIGN { 1 0 10303 214 3 1 1 }'));
ENDSEC;

DATA;
#10=MECHANICAL_DESIGN_GEOMETRIC_PRESENTATION_REPRESENTATION('',(#334),#10957);
#243=B_SPLINE_CURVE_WITH_KNOTS('',3,(#10658,#10659,#10660,#10661,#10662,
#10663,#10664,#10665,#10666,#10667,#10668,#10669,#10670,#10671,#10672,#10673,
#10674,#10675,#10676,#10677,#10678,#10679,#10680,#10681,#10682,#10683,#10684,
#10685,#10686,#10687,#10688,#10689,#10690,#10691),.UNSPECIFIED.,.T.,.F.,
(4,2,2,2,2,2,2,2,2,2,2,2,2,2,2,2,4),(0.,0.0623062782223143,0.124612556444629,
0.186916384615149,0.249220212785669,0.31152404095619,0.37382786912671,0.436134147349024,
0.498440425571339,0.560746703793653,0.623052982015967,0.685356810186488,
0.747660638357008,0.809964466527529,0.872268294698049,0.934574572920363,
0.996880851142678),.UNSPECIFIED.);
#244=B_SPLINE_CURVE_WITH_KNOTS('',3,(#10694,#10695,#10696,#10697,#10698,
#10699,#10700,#10701,#10702,#10703,#10704,#10705,#10706,#10707),
 .UNSPECIFIED.,.F.,.F.,(4,2,2,2,2,2,4),(0.618551524396292,0.626563103102765,
0.689203386094988,0.751843669087211,0.814483952079434,0.877124235071657,
0.88513581377813),.UNSPECIFIED.);
#245=B_SPLINE_CURVE_WITH_KNOTS('',3,(#10710,#10711,#10712,#10713,#10714,
#10715,#10716,#10717,#10718,#10719,#10720,#10721,#10722,#10723),
 .UNSPECIFIED.,.F.,.F.,(4,2,2,2,2,2,4),(0.117322411671484,0.125333990377958,
0.187974273370181,0.250614556362404,0.313254839354627,0.37589512234685,
0.383906701053322),.UNSPECIFIED.);
#246=B_SPLINE_CURVE_WITH_KNOTS('',3,(#10734,#10735,#10736,#10737,#10738,
#10739,#10740,#10741,#10742,#10743),.UNSPECIFIED.,.F.,.F.,(4,2,2,2,4),(0.,
0.0623062782223142,0.124612556444628,0.186916384615149,0.249220212785669),
 .UNSPECIFIED.);
#247=B_SPLINE_CURVE_WITH_KNOTS('',3,(#10745,#10746,#10747,#10748,#10749,
#10750,#10751,#10752,#10753,#10754),.UNSPECIFIED.,.F.,.F.,(4,2,2,2,4),(0.747660638357008,
0.809964466527528,0.872268294698049,0.934574572920363,0.996880851142677),
 .UNSPECIFIED.);
#248=B_SPLINE_CURVE_WITH_KNOTS('',3,(#10755,#10756,#10757,#10758,#10759,
#10760,#10761,#10762,#10763,#10764,#10765,#10766,#10767,#10768,#10769,#10770,
#10771,#10772),.UNSPECIFIED.,.F.,.F.,(4,2,2,2,2,2,2,2,4),(0.249220212785669,
0.31152404095619,0.37382786912671,0.436134147349024,0.498440425571339,0.560746703793653,
0.623052982015967,0.685356810186488,0.747660638357008),.UNSPECIFIED.);
#249=B_SPLINE_CURVE_WITH_KNOTS('',3,(#10776,#10777,#10778,#10779,#10780,
#10781,#10782,#10783),.UNSPECIFIED.,.F.,.F.,(4,2,2,4),(0.618551507245623,
0.626563103102765,0.689203386094988,0.751843669087211),.UNSPECIFIED.);
#250=B_SPLINE_CURVE_WITH_KNOTS('',3,(#10787,#10788,#10789,#10790,#10791,
#10792,#10793,#10794),.UNSPECIFIED.,.F.,.F.,(4,2,2,4),(0.250614556362404,
0.313254839354627,0.37589512234685,0.383906718203992),.UNSPECIFIED.);
#251=B_SPLINE_CURVE_WITH_KNOTS('',3,(#10795,#10796,#10797,#10798,#10799,
#10800,#10801,#10802),.UNSPECIFIED.,.F.,.F.,(4,2,2,4),(0.117322394520816,
0.125333990377958,0.187974273370181,0.250614556362404),.UNSPECIFIED.);
#252=B_SPLINE_CURVE_WITH_KNOTS('',3,(#10803,#10804,#10805,#10806,#10807,
#10808,#10809,#10810),.UNSPECIFIED.,.F.,.F.,(4,2,2,4),(0.751843669087211,
0.814483952079434,0.877124235071657,0.8851358309288),.UNSPECIFIED.);
#276=SHAPE_REPRESENTATION_RELATIONSHIP('SRR','None',#11092,#301);
#301=ADVANCED_BREP_SHAPE_REPRESENTATION('',(#365),#10955);
#334=STYLED_ITEM('',(#11301),#365);
#365=MANIFOLD_SOLID_BREP('Body1',#5732);
#467=FACE_BOUND('',#1404,.T.);
#468=FACE_BOUND('',#1406,.T.);
#469=FACE_BOUND('',#1408,.T.);
#470=FACE_BOUND('',#1410,.T.);
#637=PLANE('',#6698);
#638=PLANE('',#6703);
#639=PLANE('',#6704);
#640=PLANE('',#6708);
#641=PLANE('',#6715);
#642=PLANE('',#6716);
#964=FACE_OUTER_BOUND('',#1397,.T.);
#965=FACE_OUTER_BOUND('',#1398,.T.);
#966=FACE_OUTER_BOUND('',#1399,.T.);
#967=FACE_OUTER_BOUND('',#1400,.T.);
#968=FACE_OUTER_BOUND('',#1401,.T.);
#969=FACE_OUTER_BOUND('',#1402,.T.);
#970=FACE_OUTER_BOUND('',#1403,.T.);
#971=FACE_OUTER_BOUND('',#1405,.T.);
#972=FACE_OUTER_BOUND('',#1407,.T.);
#973=FACE_OUTER_BOUND('',#1409,.T.);
#1397=EDGE_LOOP('',(#5139,#5140,#5141));
#1398=EDGE_LOOP('',(#5142,#5143,#5144,#5145,#5146,#5147,#5148,#5149));
#1399=EDGE_LOOP('',(#5150,#5151));
#1400=EDGE_LOOP('',(#5152,#5153));
#1401=EDGE_LOOP('',(#5154,#5155,#5156,#5157,#5158,#5159,#5160,#5161,#5162,
#5163,#5164));
#1402=EDGE_LOOP('',(#5165,#5166));
#1403=EDGE_LOOP('',(#5167,#5168,#5169,#5170,#5171,#5172,#5173,#5174,#5175,
#5176,#5177,#5178));
#1404=EDGE_LOOP('',(#5179,#5180,#5181,#5182));
#1405=EDGE_LOOP('',(#5183,#5184,#5185,#5186,#5187,#5188,#5189,#5190,#5191));
#1406=EDGE_LOOP('',(#5192));
#1407=EDGE_LOOP('',(#5193));
#1408=EDGE_LOOP('',(#5194));
#1409=EDGE_LOOP('',(#5195));
#1410=EDGE_LOOP('',(#5196));
#1767=LINE('',#10652,#2141);
#1768=LINE('',#10692,#2142);
#1769=LINE('',#10725,#2143);
#1770=LINE('',#10729,#2144);
#1771=LINE('',#10774,#2145);
#1772=LINE('',#10812,#2146);
#1773=LINE('',#10816,#2147);
#1774=LINE('',#10818,#2148);
#1775=LINE('',#10823,#2149);
#1776=LINE('',#10825,#2150);
#2141=VECTOR('',#8471,1.);
#2142=VECTOR('',#8478,0.165);
#2143=VECTOR('',#8483,1.);
#2144=VECTOR('',#8486,1.);
#2145=VECTOR('',#8491,0.165);
#2146=VECTOR('',#8496,1.);
#2147=VECTOR('',#8501,0.505);
#2148=VECTOR('',#8502,0.505);
#2149=VECTOR('',#8509,0.9);
#2150=VECTOR('',#8510,0.9);
#2493=CIRCLE('',#6699,0.165);
#2494=CIRCLE('',#6700,0.165);
#2495=CIRCLE('',#6702,0.165);
#2496=CIRCLE('',#6705,0.165);
#2497=CIRCLE('',#6707,0.165);
#2498=CIRCLE('',#6710,0.505);
#2499=CIRCLE('',#6711,0.505);
#2500=CIRCLE('',#6713,0.9);
#2501=CIRCLE('',#6714,0.9);
#2965=VERTEX_POINT('',#10650);
#2966=VERTEX_POINT('',#10651);
#2967=VERTEX_POINT('',#10653);
#2968=VERTEX_POINT('',#10657);
#2969=VERTEX_POINT('',#10693);
#2970=VERTEX_POINT('',#10708);
#2971=VERTEX_POINT('',#10727);
#2972=VERTEX_POINT('',#10728);
#2973=VERTEX_POINT('',#10732);
#2974=VERTEX_POINT('',#10733);
#2975=VERTEX_POINT('',#10744);
#2976=VERTEX_POINT('',#10773);
#2977=VERTEX_POINT('',#10775);
#2978=VERTEX_POINT('',#10784);
#2979=VERTEX_POINT('',#10786);
#2980=VERTEX_POINT('',#10814);
#2981=VERTEX_POINT('',#10817);
#2982=VERTEX_POINT('',#10821);
#2983=VERTEX_POINT('',#10824);
#3695=EDGE_CURVE('',#2965,#2966,#1767,.T.);
#3696=EDGE_CURVE('',#2967,#2965,#2493,.T.);
#3697=EDGE_CURVE('',#2966,#2967,#2494,.T.);
#3698=EDGE_CURVE('',#2968,#2968,#243,.T.);
#3699=EDGE_CURVE('',#2968,#2967,#1768,.T.);
#3700=EDGE_CURVE('',#2969,#2965,#244,.T.);
#3701=EDGE_CURVE('',#2969,#2970,#2495,.T.);
#3702=EDGE_CURVE('',#2966,#2970,#245,.T.);
#3703=EDGE_CURVE('',#2970,#2969,#1769,.T.);
#3704=EDGE_CURVE('',#2971,#2972,#1770,.T.);
#3705=EDGE_CURVE('',#2972,#2971,#2496,.T.);
#3706=EDGE_CURVE('',#2973,#2974,#246,.T.);
#3707=EDGE_CURVE('',#2975,#2973,#247,.T.);
#3708=EDGE_CURVE('',#2974,#2975,#248,.T.);
#3709=EDGE_CURVE('',#2974,#2976,#1771,.T.);
#3710=EDGE_CURVE('',#2977,#2976,#249,.T.);
#3711=EDGE_CURVE('',#2977,#2978,#2497,.T.);
#3712=EDGE_CURVE('',#2979,#2978,#250,.T.);
#3713=EDGE_CURVE('',#2972,#2979,#251,.T.);
#3714=EDGE_CURVE('',#2976,#2971,#252,.T.);
#3715=EDGE_CURVE('',#2978,#2977,#1772,.T.);
#3716=EDGE_CURVE('',#2980,#2980,#2498,.T.);
#3717=EDGE_CURVE('',#2980,#2976,#1773,.T.);
#3718=EDGE_CURVE('',#2979,#2981,#1774,.T.);
#3719=EDGE_CURVE('',#2981,#2981,#2499,.T.);
#3720=EDGE_CURVE('',#2982,#2982,#2500,.T.);
#3721=EDGE_CURVE('',#2982,#2974,#1775,.T.);
#3722=EDGE_CURVE('',#2975,#2983,#1776,.T.);
#3723=EDGE_CURVE('',#2983,#2983,#2501,.T.);
#5139=ORIENTED_EDGE('',*,*,#3695,.F.);
#5140=ORIENTED_EDGE('',*,*,#3696,.F.);
#5141=ORIENTED_EDGE('',*,*,#3697,.F.);
#5142=ORIENTED_EDGE('',*,*,#3698,.F.);
#5143=ORIENTED_EDGE('',*,*,#3699,.T.);
#5144=ORIENTED_EDGE('',*,*,#3696,.T.);
#5145=ORIENTED_EDGE('',*,*,#3700,.F.);
#5146=ORIENTED_EDGE('',*,*,#3701,.T.);
#5147=ORIENTED_EDGE('',*,*,#3702,.F.);
#5148=ORIENTED_EDGE('',*,*,#3697,.T.);
#5149=ORIENTED_EDGE('',*,*,#3699,.F.);
#5150=ORIENTED_EDGE('',*,*,#3703,.F.);
#5151=ORIENTED_EDGE('',*,*,#3701,.F.);
#5152=ORIENTED_EDGE('',*,*,#3704,.F.);
#5153=ORIENTED_EDGE('',*,*,#3705,.F.);
#5154=ORIENTED_EDGE('',*,*,#3706,.F.);
#5155=ORIENTED_EDGE('',*,*,#3707,.F.);
#5156=ORIENTED_EDGE('',*,*,#3708,.F.);
#5157=ORIENTED_EDGE('',*,*,#3709,.T.);
#5158=ORIENTED_EDGE('',*,*,#3710,.F.);
#5159=ORIENTED_EDGE('',*,*,#3711,.T.);
#5160=ORIENTED_EDGE('',*,*,#3712,.F.);
#5161=ORIENTED_EDGE('',*,*,#3713,.F.);
#5162=ORIENTED_EDGE('',*,*,#3705,.T.);
#5163=ORIENTED_EDGE('',*,*,#3714,.F.);
#5164=ORIENTED_EDGE('',*,*,#3709,.F.);
#5165=ORIENTED_EDGE('',*,*,#3715,.F.);
#5166=ORIENTED_EDGE('',*,*,#3711,.F.);
#5167=ORIENTED_EDGE('',*,*,#3716,.F.);
#5168=ORIENTED_EDGE('',*,*,#3717,.T.);
#5169=ORIENTED_EDGE('',*,*,#3714,.T.);
#5170=ORIENTED_EDGE('',*,*,#3704,.T.);
#5171=ORIENTED_EDGE('',*,*,#3713,.T.);
#5172=ORIENTED_EDGE('',*,*,#3718,.T.);
#5173=ORIENTED_EDGE('',*,*,#3719,.T.);
#5174=ORIENTED_EDGE('',*,*,#3718,.F.);
#5175=ORIENTED_EDGE('',*,*,#3712,.T.);
#5176=ORIENTED_EDGE('',*,*,#3715,.T.);
#5177=ORIENTED_EDGE('',*,*,#3710,.T.);
#5178=ORIENTED_EDGE('',*,*,#3717,.F.);
#5179=ORIENTED_EDGE('',*,*,#3702,.T.);
#5180=ORIENTED_EDGE('',*,*,#3703,.T.);
#5181=ORIENTED_EDGE('',*,*,#3700,.T.);
#5182=ORIENTED_EDGE('',*,*,#3695,.T.);
#5183=ORIENTED_EDGE('',*,*,#3720,.F.);
#5184=ORIENTED_EDGE('',*,*,#3721,.T.);
#5185=ORIENTED_EDGE('',*,*,#3708,.T.);
#5186=ORIENTED_EDGE('',*,*,#3722,.T.);
#5187=ORIENTED_EDGE('',*,*,#3723,.T.);
#5188=ORIENTED_EDGE('',*,*,#3722,.F.);
#5189=ORIENTED_EDGE('',*,*,#3707,.T.);
#5190=ORIENTED_EDGE('',*,*,#3706,.T.);
#5191=ORIENTED_EDGE('',*,*,#3721,.F.);
#5192=ORIENTED_EDGE('',*,*,#3698,.T.);
#5193=ORIENTED_EDGE('',*,*,#3720,.T.);
#5194=ORIENTED_EDGE('',*,*,#3716,.T.);
#5195=ORIENTED_EDGE('',*,*,#3723,.F.);
#5196=ORIENTED_EDGE('',*,*,#3719,.F.);
#5361=CYLINDRICAL_SURFACE('',#6701,0.165);
#5362=CYLINDRICAL_SURFACE('',#6706,0.165);
#5363=CYLINDRICAL_SURFACE('',#6709,0.505);
#5364=CYLINDRICAL_SURFACE('',#6712,0.9);
#5678=ADVANCED_FACE('',(#964),#637,.F.);
#5679=ADVANCED_FACE('',(#965),#5361,.F.);
#5680=ADVANCED_FACE('',(#966),#638,.F.);
#5681=ADVANCED_FACE('',(#967),#639,.F.);
#5682=ADVANCED_FACE('',(#968),#5362,.F.);
#5683=ADVANCED_FACE('',(#969),#640,.F.);
#5684=ADVANCED_FACE('',(#970,#467),#5363,.F.);
#5685=ADVANCED_FACE('',(#971,#468),#5364,.T.);
#5686=ADVANCED_FACE('',(#972,#469),#641,.T.);
#5687=ADVANCED_FACE('',(#973,#470),#642,.F.);
#5732=CLOSED_SHELL('',(#5678,#5679,#5680,#5681,#5682,#5683,#5684,#5685,
#5686,#5687));
#6697=AXIS2_PLACEMENT_3D('',#10648,#8467,#8468);
#6698=AXIS2_PLACEMENT_3D('',#10649,#8469,#8470);
#6699=AXIS2_PLACEMENT_3D('',#10654,#8472,#8473);
#6700=AXIS2_PLACEMENT_3D('',#10655,#8474,#8475);
#6701=AXIS2_PLACEMENT_3D('',#10656,#8476,#8477);
#6702=AXIS2_PLACEMENT_3D('',#10709,#8479,#8480);
#6703=AXIS2_PLACEMENT_3D('',#10724,#8481,#8482);
#6704=AXIS2_PLACEMENT_3D('',#10726,#8484,#8485);
#6705=AXIS2_PLACEMENT_3D('',#10730,#8487,#8488);
#6706=AXIS2_PLACEMENT_3D('',#10731,#8489,#8490);
#6707=AXIS2_PLACEMENT_3D('',#10785,#8492,#8493);
#6708=AXIS2_PLACEMENT_3D('',#10811,#8494,#8495);
#6709=AXIS2_PLACEMENT_3D('',#10813,#8497,#8498);
#6710=AXIS2_PLACEMENT_3D('',#10815,#8499,#8500);
#6711=AXIS2_PLACEMENT_3D('',#10819,#8503,#8504);
#6712=AXIS2_PLACEMENT_3D('',#10820,#8505,#8506);
#6713=AXIS2_PLACEMENT_3D('',#10822,#8507,#8508);
#6714=AXIS2_PLACEMENT_3D('',#10826,#8511,#8512);
#6715=AXIS2_PLACEMENT_3D('',#10827,#8513,#8514);
#6716=AXIS2_PLACEMENT_3D('',#10828,#8515,#8516);
#8467=DIRECTION('axis',(0.,0.,1.));
#8468=DIRECTION('refdir',(1.,0.,0.));
#8469=DIRECTION('center_axis',(0.,1.,0.));
#8470=DIRECTION('ref_axis',(1.,0.,0.));
#8471=DIRECTION('',(0.,0.,-1.));
#8472=DIRECTION('center_axis',(0.,1.,0.));
#8473=DIRECTION('ref_axis',(1.,0.,0.));
#8474=DIRECTION('center_axis',(0.,1.,0.));
#8475=DIRECTION('ref_axis',(1.,0.,0.));
#8476=DIRECTION('center_axis',(0.,1.,0.));
#8477=DIRECTION('ref_axis',(1.,0.,0.));
#8478=DIRECTION('',(0.,1.,0.));
#8479=DIRECTION('center_axis',(0.,1.,0.));
#8480=DIRECTION('ref_axis',(1.,0.,0.));
#8481=DIRECTION('center_axis',(0.,1.,0.));
#8482=DIRECTION('ref_axis',(1.,0.,0.));
#8483=DIRECTION('',(0.,0.,1.));
#8484=DIRECTION('center_axis',(1.,0.,0.));
#8485=DIRECTION('ref_axis',(0.,0.,-1.));
#8486=DIRECTION('',(0.,0.,-1.));
#8487=DIRECTION('center_axis',(1.,0.,0.));
#8488=DIRECTION('ref_axis',(0.,0.,-1.));
#8489=DIRECTION('center_axis',(1.,0.,0.));
#8490=DIRECTION('ref_axis',(0.,0.,-1.));
#8491=DIRECTION('',(1.,0.,0.));
#8492=DIRECTION('center_axis',(1.,0.,0.));
#8493=DIRECTION('ref_axis',(0.,0.,-1.));
#8494=DIRECTION('center_axis',(1.,0.,0.));
#8495=DIRECTION('ref_axis',(0.,0.,-1.));
#8496=DIRECTION('',(0.,0.,1.));
#8497=DIRECTION('center_axis',(0.,0.,1.));
#8498=DIRECTION('ref_axis',(1.,0.,0.));
#8499=DIRECTION('center_axis',(0.,0.,-1.));
#8500=DIRECTION('ref_axis',(1.,0.,0.));
#8501=DIRECTION('',(0.,0.,-1.));
#8502=DIRECTION('',(0.,0.,-1.));
#8503=DIRECTION('center_axis',(0.,0.,-1.));
#8504=DIRECTION('ref_axis',(1.,0.,0.));
#8505=DIRECTION('center_axis',(0.,0.,1.));
#8506=DIRECTION('ref_axis',(1.,0.,0.));
#8507=DIRECTION('center_axis',(0.,0.,1.));
#8508=DIRECTION('ref_axis',(1.,0.,0.));
#8509=DIRECTION('',(0.,0.,-1.));
#8510=DIRECTION('',(0.,0.,-1.));
#8511=DIRECTION('center_axis',(0.,0.,1.));
#8512=DIRECTION('ref_axis',(1.,0.,0.));
#8513=DIRECTION('center_axis',(0.,0.,1.));
#8514=DIRECTION('ref_axis',(1.,0.,0.));
#8515=DIRECTION('center_axis',(0.,0.,1.));
#8516=DIRECTION('ref_axis',(1.,0.,0.));
#10648=CARTESIAN_POINT('',(0.,0.,0.));
#10649=CARTESIAN_POINT('Origin',(4.24264068711929,-0.49,1.4));
#10650=CARTESIAN_POINT('',(4.12047276989058,-0.49,1.51090536506409));
#10651=CARTESIAN_POINT('',(4.12047276989058,-0.49,1.28909463493591));
#10652=CARTESIAN_POINT('',(4.12047276989058,-0.49,1.));
#10653=CARTESIAN_POINT('',(4.07764068711929,-0.49,1.4));
#10654=CARTESIAN_POINT('Origin',(4.24264068711929,-0.49,1.4));
#10655=CARTESIAN_POINT('Origin',(4.24264068711929,-0.49,1.4));
#10656=CARTESIAN_POINT('Origin',(4.24264068711929,-1.,1.4));
#10657=CARTESIAN_POINT('',(4.07764068711929,-0.884745726183518,1.4));
#10658=CARTESIAN_POINT('Ctrl Pts',(4.07764068711929,-0.884745726183518,
1.4));
#10659=CARTESIAN_POINT('Ctrl Pts',(4.07764068711929,-0.884745726183518,
1.42076875940744));
#10660=CARTESIAN_POINT('Ctrl Pts',(4.0818009681117,-0.885552759505265,1.44288889507334));
#10661=CARTESIAN_POINT('Ctrl Pts',(4.0986542169026,-0.888448648150043,1.48352706263377));
#10662=CARTESIAN_POINT('Ctrl Pts',(4.1113446933051,-0.890493604851638,1.50204924397737));
#10663=CARTESIAN_POINT('Ctrl Pts',(4.14059086811116,-0.894317234323941,
1.53129541878344));
#10664=CARTESIAN_POINT('Ctrl Pts',(4.1591132950286,-0.896347088899543,1.54398634598358));
#10665=CARTESIAN_POINT('Ctrl Pts',(4.19975231102587,-0.899208271860583,
1.56083992183864));
#10666=CARTESIAN_POINT('Ctrl Pts',(4.22187274439578,-0.9,1.565));
#10667=CARTESIAN_POINT('Ctrl Pts',(4.26340862984279,-0.9,1.565));
#10668=CARTESIAN_POINT('Ctrl Pts',(4.2855290632127,-0.899208271860583,1.56083992183864));
#10669=CARTESIAN_POINT('Ctrl Pts',(4.32616807920997,-0.896347088899543,
1.54398634598358));
#10670=CARTESIAN_POINT('Ctrl Pts',(4.34469050612741,-0.894317234323941,
1.53129541878344));
#10671=CARTESIAN_POINT('Ctrl Pts',(4.37393668093347,-0.890493604851638,
1.50204924397737));
#10672=CARTESIAN_POINT('Ctrl Pts',(4.38662715733598,-0.888448648150043,
1.48352706263377));
#10673=CARTESIAN_POINT('Ctrl Pts',(4.40348040612687,-0.885552759505265,
1.44288889507334));
#10674=CARTESIAN_POINT('Ctrl Pts',(4.40764068711929,-0.884745726183518,
1.42076875940744));
#10675=CARTESIAN_POINT('Ctrl Pts',(4.40764068711929,-0.884745726183518,
1.37923124059256));
#10676=CARTESIAN_POINT('Ctrl Pts',(4.40348040612687,-0.885552759505265,
1.35711110492666));
#10677=CARTESIAN_POINT('Ctrl Pts',(4.38662715733598,-0.888448648150043,
1.31647293736623));
#10678=CARTESIAN_POINT('Ctrl Pts',(4.37393668093347,-0.890493604851638,
1.29795075602263));
#10679=CARTESIAN_POINT('Ctrl Pts',(4.34469050612741,-0.894317234323941,
1.26870458121656));
#10680=CARTESIAN_POINT('Ctrl Pts',(4.32616807920997,-0.896347088899543,
1.25601365401642));
#10681=CARTESIAN_POINT('Ctrl Pts',(4.2855290632127,-0.899208271860583,1.23916007816136));
#10682=CARTESIAN_POINT('Ctrl Pts',(4.26340862984279,-0.9,1.235));
#10683=CARTESIAN_POINT('Ctrl Pts',(4.22187274439578,-0.9,1.235));
#10684=CARTESIAN_POINT('Ctrl Pts',(4.19975231102587,-0.899208271860583,
1.23916007816136));
#10685=CARTESIAN_POINT('Ctrl Pts',(4.1591132950286,-0.896347088899543,1.25601365401642));
#10686=CARTESIAN_POINT('Ctrl Pts',(4.14059086811116,-0.894317234323941,
1.26870458121656));
#10687=CARTESIAN_POINT('Ctrl Pts',(4.1113446933051,-0.890493604851638,1.29795075602263));
#10688=CARTESIAN_POINT('Ctrl Pts',(4.0986542169026,-0.888448648150043,1.31647293736623));
#10689=CARTESIAN_POINT('Ctrl Pts',(4.0818009681117,-0.885552759505265,1.35711110492666));
#10690=CARTESIAN_POINT('Ctrl Pts',(4.07764068711929,-0.884745726183518,
1.37923124059256));
#10691=CARTESIAN_POINT('Ctrl Pts',(4.07764068711929,-0.884745726183518,
1.4));
#10692=CARTESIAN_POINT('',(4.07764068711929,-1.,1.4));
#10693=CARTESIAN_POINT('',(4.36480860434799,-0.49,1.51090536506409));
#10694=CARTESIAN_POINT('Ctrl Pts',(4.36480860434799,-0.49,1.51090536506409));
#10695=CARTESIAN_POINT('Ctrl Pts',(4.36300960074558,-0.490448531679987,
1.51288705930464));
#10696=CARTESIAN_POINT('Ctrl Pts',(4.36117558368452,-0.490895245371684,
1.51481034122633));
#10697=CARTESIAN_POINT('Ctrl Pts',(4.34475268013864,-0.494795015531646,
1.5312332447722));
#10698=CARTESIAN_POINT('Ctrl Pts',(4.32630040214172,-0.498442514607594,
1.54390845611142));
#10699=CARTESIAN_POINT('Ctrl Pts',(4.28569028316644,-0.50357781976106,1.56079590960766));
#10700=CARTESIAN_POINT('Ctrl Pts',(4.26352078145003,-0.505,1.565));
#10701=CARTESIAN_POINT('Ctrl Pts',(4.22176059278855,-0.505,1.565));
#10702=CARTESIAN_POINT('Ctrl Pts',(4.19959109107213,-0.50357781976106,1.56079590960766));
#10703=CARTESIAN_POINT('Ctrl Pts',(4.15898097209685,-0.498442514607594,
1.54390845611142));
#10704=CARTESIAN_POINT('Ctrl Pts',(4.14052869409993,-0.494795015531646,
1.5312332447722));
#10705=CARTESIAN_POINT('Ctrl Pts',(4.12410579055406,-0.490895245371684,
1.51481034122633));
#10706=CARTESIAN_POINT('Ctrl Pts',(4.12227177349299,-0.490448531679987,
1.51288705930464));
#10707=CARTESIAN_POINT('Ctrl Pts',(4.12047276989058,-0.49,1.51090536506409));
#10708=CARTESIAN_POINT('',(4.36480860434799,-0.49,1.28909463493591));
#10709=CARTESIAN_POINT('Origin',(4.24264068711929,-0.49,1.4));
#10710=CARTESIAN_POINT('Ctrl Pts',(4.12047276989058,-0.49,1.28909463493591));
#10711=CARTESIAN_POINT('Ctrl Pts',(4.12227177349299,-0.490448531679987,
1.28711294069536));
#10712=CARTESIAN_POINT('Ctrl Pts',(4.12410579055406,-0.490895245371684,
1.28518965877367));
#10713=CARTESIAN_POINT('Ctrl Pts',(4.14052869409993,-0.494795015531646,
1.2687667552278));
#10714=CARTESIAN_POINT('Ctrl Pts',(4.15898097209685,-0.498442514607594,
1.25609154388858));
#10715=CARTESIAN_POINT('Ctrl Pts',(4.19959109107213,-0.50357781976106,1.23920409039234));
#10716=CARTESIAN_POINT('Ctrl Pts',(4.22176059278855,-0.505,1.235));
#10717=CARTESIAN_POINT('Ctrl Pts',(4.26352078145003,-0.505,1.235));
#10718=CARTESIAN_POINT('Ctrl Pts',(4.28569028316644,-0.50357781976106,1.23920409039234));
#10719=CARTESIAN_POINT('Ctrl Pts',(4.32630040214172,-0.498442514607594,
1.25609154388858));
#10720=CARTESIAN_POINT('Ctrl Pts',(4.34475268013864,-0.494795015531646,
1.2687667552278));
#10721=CARTESIAN_POINT('Ctrl Pts',(4.36117558368452,-0.490895245371684,
1.28518965877367));
#10722=CARTESIAN_POINT('Ctrl Pts',(4.36300960074558,-0.490448531679987,
1.28711294069536));
#10723=CARTESIAN_POINT('Ctrl Pts',(4.36480860434799,-0.49,1.28909463493591));
#10724=CARTESIAN_POINT('Origin',(4.24264068711929,-0.49,1.4));
#10725=CARTESIAN_POINT('',(4.36480860434799,-0.49,1.));
#10726=CARTESIAN_POINT('Origin',(3.75264069,0.,1.4));
#10727=CARTESIAN_POINT('',(3.75264069,0.122167928782887,1.51090535233657));
#10728=CARTESIAN_POINT('',(3.75264069,0.122167928782887,1.28909464766343));
#10729=CARTESIAN_POINT('',(3.75264069,0.122167928782887,1.));
#10730=CARTESIAN_POINT('Origin',(3.75264069,0.,1.4));
#10731=CARTESIAN_POINT('Origin',(3.24264069,0.,1.4));
#10732=CARTESIAN_POINT('',(3.35789496093577,0.165,1.4));
#10733=CARTESIAN_POINT('',(3.34264068711929,-2.02066721859313E-17,1.565));
#10734=CARTESIAN_POINT('Ctrl Pts',(3.35789496093577,0.165,1.4));
#10735=CARTESIAN_POINT('Ctrl Pts',(3.35789496093577,0.165,1.42076875940744));
#10736=CARTESIAN_POINT('Ctrl Pts',(3.35708792761402,0.160839719007584,1.44288889507334));
#10737=CARTESIAN_POINT('Ctrl Pts',(3.35419203896924,0.143986470216691,1.48352706263377));
#10738=CARTESIAN_POINT('Ctrl Pts',(3.35214708226765,0.131295993814186,1.50204924397737));
#10739=CARTESIAN_POINT('Ctrl Pts',(3.34832345279534,0.102049819008125,1.53129541878344));
#10740=CARTESIAN_POINT('Ctrl Pts',(3.34629359821974,0.0835273920906824,
1.54398634598358));
#10741=CARTESIAN_POINT('Ctrl Pts',(3.3434324152587,0.0428883760934127,1.56083992183864));
#10742=CARTESIAN_POINT('Ctrl Pts',(3.34264068711929,0.0207679427235068,
1.565));
#10743=CARTESIAN_POINT('Ctrl Pts',(3.34264068711929,2.77555756156289E-17,
1.565));
#10744=CARTESIAN_POINT('',(3.34264068711929,-7.59257876733526E-17,1.235));
#10745=CARTESIAN_POINT('Ctrl Pts',(3.34264068711929,-4.16333634234434E-17,
1.235));
#10746=CARTESIAN_POINT('Ctrl Pts',(3.34264068711929,0.0207679427235068,
1.235));
#10747=CARTESIAN_POINT('Ctrl Pts',(3.3434324152587,0.0428883760934127,1.23916007816136));
#10748=CARTESIAN_POINT('Ctrl Pts',(3.34629359821974,0.0835273920906823,
1.25601365401642));
#10749=CARTESIAN_POINT('Ctrl Pts',(3.34832345279534,0.102049819008125,1.26870458121656));
#10750=CARTESIAN_POINT('Ctrl Pts',(3.35214708226765,0.131295993814186,1.29795075602263));
#10751=CARTESIAN_POINT('Ctrl Pts',(3.35419203896924,0.143986470216691,1.31647293736623));
#10752=CARTESIAN_POINT('Ctrl Pts',(3.35708792761402,0.160839719007584,1.35711110492666));
#10753=CARTESIAN_POINT('Ctrl Pts',(3.35789496093577,0.165,1.37923124059256));
#10754=CARTESIAN_POINT('Ctrl Pts',(3.35789496093577,0.165,1.4));
#10755=CARTESIAN_POINT('Ctrl Pts',(3.34264068711929,2.77555756156289E-17,
1.565));
#10756=CARTESIAN_POINT('Ctrl Pts',(3.34264068711929,-0.0207679427235068,
1.565));
#10757=CARTESIAN_POINT('Ctrl Pts',(3.3434324152587,-0.0428883760934127,
1.56083992183864));
#10758=CARTESIAN_POINT('Ctrl Pts',(3.34629359821974,-0.0835273920906823,
1.54398634598358));
#10759=CARTESIAN_POINT('Ctrl Pts',(3.34832345279534,-0.102049819008125,
1.53129541878344));
#10760=CARTESIAN_POINT('Ctrl Pts',(3.35214708226765,-0.131295993814186,
1.50204924397737));
#10761=CARTESIAN_POINT('Ctrl Pts',(3.35419203896924,-0.143986470216691,
1.48352706263377));
#10762=CARTESIAN_POINT('Ctrl Pts',(3.35708792761402,-0.160839719007584,
1.44288889507334));
#10763=CARTESIAN_POINT('Ctrl Pts',(3.35789496093577,-0.165,1.42076875940744));
#10764=CARTESIAN_POINT('Ctrl Pts',(3.35789496093577,-0.165,1.37923124059256));
#10765=CARTESIAN_POINT('Ctrl Pts',(3.35708792761402,-0.160839719007584,
1.35711110492666));
#10766=CARTESIAN_POINT('Ctrl Pts',(3.35419203896924,-0.143986470216691,
1.31647293736623));
#10767=CARTESIAN_POINT('Ctrl Pts',(3.35214708226765,-0.131295993814186,
1.29795075602263));
#10768=CARTESIAN_POINT('Ctrl Pts',(3.34832345279534,-0.102049819008125,
1.26870458121656));
#10769=CARTESIAN_POINT('Ctrl Pts',(3.34629359821974,-0.0835273920906824,
1.25601365401642));
#10770=CARTESIAN_POINT('Ctrl Pts',(3.3434324152587,-0.0428883760934128,
1.23916007816136));
#10771=CARTESIAN_POINT('Ctrl Pts',(3.34264068711929,-0.0207679427235068,
1.235));
#10772=CARTESIAN_POINT('Ctrl Pts',(3.34264068711929,-4.16333634234434E-17,
1.235));
#10773=CARTESIAN_POINT('',(3.73764068711929,-1.70422299968729E-17,1.565));
#10774=CARTESIAN_POINT('',(3.24264069,-2.02066721859313E-17,1.565));
#10775=CARTESIAN_POINT('',(3.75264069,-0.122167928782887,1.51090535233657));
#10776=CARTESIAN_POINT('Ctrl Pts',(3.75264069,-0.122167928782887,1.51090535233657));
#10777=CARTESIAN_POINT('Ctrl Pts',(3.75219215735201,-0.120368921478644,
1.51288705106972));
#10778=CARTESIAN_POINT('Ctrl Pts',(3.75174544269427,-0.118534900551874,
1.51481033723969));
#10779=CARTESIAN_POINT('Ctrl Pts',(3.74784567158764,-0.102111993019358,
1.5312332447722));
#10780=CARTESIAN_POINT('Ctrl Pts',(3.74419817251169,-0.0836597150224319,
1.54390845611142));
#10781=CARTESIAN_POINT('Ctrl Pts',(3.73906286735823,-0.0430495960471595,
1.56079590960766));
#10782=CARTESIAN_POINT('Ctrl Pts',(3.73764068711929,-0.020880094330741,
1.565));
#10783=CARTESIAN_POINT('Ctrl Pts',(3.73764068711929,-2.08166817117217E-17,
1.565));
#10784=CARTESIAN_POINT('',(3.75264069,-0.122167928782887,1.28909464766343));
#10785=CARTESIAN_POINT('Origin',(3.75264069,0.,1.4));
#10786=CARTESIAN_POINT('',(3.73764068711929,-3.09223316784707E-17,1.235));
#10787=CARTESIAN_POINT('Ctrl Pts',(3.73764068711929,-1.38777878078145E-17,
1.235));
#10788=CARTESIAN_POINT('Ctrl Pts',(3.73764068711929,-0.020880094330741,
1.235));
#10789=CARTESIAN_POINT('Ctrl Pts',(3.73906286735823,-0.0430495960471595,
1.23920409039234));
#10790=CARTESIAN_POINT('Ctrl Pts',(3.74419817251169,-0.0836597150224319,
1.25609154388858));
#10791=CARTESIAN_POINT('Ctrl Pts',(3.74784567158764,-0.102111993019358,
1.2687667552278));
#10792=CARTESIAN_POINT('Ctrl Pts',(3.75174544269427,-0.118534900551874,
1.28518966276031));
#10793=CARTESIAN_POINT('Ctrl Pts',(3.75219215735201,-0.120368921478644,
1.28711294893028));
#10794=CARTESIAN_POINT('Ctrl Pts',(3.75264069,-0.122167928782887,1.28909464766343));
#10795=CARTESIAN_POINT('Ctrl Pts',(3.75264069,0.122167928782887,1.28909464766343));
#10796=CARTESIAN_POINT('Ctrl Pts',(3.75219215735201,0.120368921478644,1.28711294893028));
#10797=CARTESIAN_POINT('Ctrl Pts',(3.75174544269427,0.118534900551874,1.28518966276031));
#10798=CARTESIAN_POINT('Ctrl Pts',(3.74784567158764,0.102111993019358,1.2687667552278));
#10799=CARTESIAN_POINT('Ctrl Pts',(3.74419817251169,0.0836597150224319,
1.25609154388858));
#10800=CARTESIAN_POINT('Ctrl Pts',(3.73906286735823,0.0430495960471595,
1.23920409039234));
#10801=CARTESIAN_POINT('Ctrl Pts',(3.73764068711929,0.020880094330741,1.235));
#10802=CARTESIAN_POINT('Ctrl Pts',(3.73764068711929,0.,1.235));
#10803=CARTESIAN_POINT('Ctrl Pts',(3.73764068711929,-6.93889390390723E-18,
1.565));
#10804=CARTESIAN_POINT('Ctrl Pts',(3.73764068711929,0.020880094330741,1.565));
#10805=CARTESIAN_POINT('Ctrl Pts',(3.73906286735823,0.0430495960471595,
1.56079590960766));
#10806=CARTESIAN_POINT('Ctrl Pts',(3.74419817251169,0.0836597150224318,
1.54390845611142));
#10807=CARTESIAN_POINT('Ctrl Pts',(3.74784567158764,0.102111993019358,1.5312332447722));
#10808=CARTESIAN_POINT('Ctrl Pts',(3.75174544269427,0.118534900551874,1.51481033723969));
#10809=CARTESIAN_POINT('Ctrl Pts',(3.75219215735201,0.120368921478644,1.51288705106972));
#10810=CARTESIAN_POINT('Ctrl Pts',(3.75264069,0.122167928782887,1.51090535233657));
#10811=CARTESIAN_POINT('Origin',(3.75264069,0.,1.4));
#10812=CARTESIAN_POINT('',(3.75264069,-0.122167928782887,1.));
#10813=CARTESIAN_POINT('Origin',(4.24264068711929,0.,1.));
#10814=CARTESIAN_POINT('',(3.73764068711929,-6.18446633569413E-17,1.8));
#10815=CARTESIAN_POINT('Origin',(4.24264068711929,0.,1.8));
#10816=CARTESIAN_POINT('',(3.73764068711929,-6.18446633569413E-17,1.));
#10817=CARTESIAN_POINT('',(3.73764068711929,-6.18446633569413E-17,1.));
#10818=CARTESIAN_POINT('',(3.73764068711929,-6.18446633569413E-17,1.));
#10819=CARTESIAN_POINT('Origin',(4.24264068711929,0.,1.));
#10820=CARTESIAN_POINT('Origin',(4.24264068711929,0.,1.));
#10821=CARTESIAN_POINT('',(3.34264068711929,-1.10218211923262E-16,1.8));
#10822=CARTESIAN_POINT('Origin',(4.24264068711929,0.,1.8));
#10823=CARTESIAN_POINT('',(3.34264068711929,-1.10218211923262E-16,1.));
#10824=CARTESIAN_POINT('',(3.34264068711929,-1.10218211923262E-16,1.));
#10825=CARTESIAN_POINT('',(3.34264068711929,-1.10218211923262E-16,1.));
#10826=CARTESIAN_POINT('Origin',(4.24264068711929,0.,1.));
#10827=CARTESIAN_POINT('Origin',(4.24264068711929,0.,1.8));
#10828=CARTESIAN_POINT('Origin',(4.24264068711929,0.,1.));
#10924=UNCERTAINTY_MEASURE_WITH_UNIT(LENGTH_MEASURE(0.001),#10958,
'DISTANCE_ACCURACY_VALUE',
'Maximum model space distance between geometric entities at asserted c
onnectivities');
#10926=UNCERTAINTY_MEASURE_WITH_UNIT(LENGTH_MEASURE(0.001),#10958,
'DISTANCE_ACCURACY_VALUE',
'Maximum model space distance between geometric entities at asserted c
onnectivities');
#10955=(
GEOMETRIC_REPRESENTATION_CONTEXT(3)
GLOBAL_UNCERTAINTY_ASSIGNED_CONTEXT((#10924))
GLOBAL_UNIT_ASSIGNED_CONTEXT((#10958,#10960,#10961))
REPRESENTATION_CONTEXT('','3D')
);
#10957=(
GEOMETRIC_REPRESENTATION_CONTEXT(3)
GLOBAL_UNCERTAINTY_ASSIGNED_CONTEXT((#10926))
GLOBAL_UNIT_ASSIGNED_CONTEXT((#10958,#10960,#10961))
REPRESENTATION_CONTEXT('','3D')
);
#10958=(
LENGTH_UNIT()
NAMED_UNIT(*)
SI_UNIT(.CENTI.,.METRE.)
);
#10960=(
NAMED_UNIT(*)
PLANE_ANGLE_UNIT()
SI_UNIT($,.RADIAN.)
);
#10961=(
NAMED_UNIT(*)
SI_UNIT($,.STERADIAN.)
SOLID_ANGLE_UNIT()
);
#10990=SHAPE_DEFINITION_REPRESENTATION(#11045,#11092);
#11045=PRODUCT_DEFINITION_SHAPE('',$,#11123);
#11092=SHAPE_REPRESENTATION('',(#6697),#10955);
#11094=PRODUCT_DEFINITION_CONTEXT('part definition',#11186,'design');
#11123=PRODUCT_DEFINITION('Retaining collar (1)','Retaining collar (1)',#11153,
#11094);
#11153=PRODUCT_DEFINITION_FORMATION('',$,#11216);
#11186=APPLICATION_CONTEXT(
'Core Data for Automotive Mechanical Design Process');
#11187=PRODUCT_CONTEXT('part definition',#11186,'mechanical');
#11216=PRODUCT('Retaining collar (1)','Retaining collar (1)',
'Retaining collar (1)',(#11187));
#11295=COLOUR_RGB('Off White',0.89,0.88,0.83);
#11296=FILL_AREA_STYLE_COLOUR('',#11295);
#11297=FILL_AREA_STYLE('',(#11296));
#11298=SURFACE_STYLE_FILL_AREA(#11297);
#11299=SURFACE_SIDE_STYLE('',(#11298));
#11300=SURFACE_STYLE_USAGE(.BOTH.,#11299);
#11301=PRESENTATION_STYLE_ASSIGNMENT((#11300));
ENDSEC;
END-ISO-10303-21;
